ISO-10303-21;
HEADER;
FILE_DESCRIPTION (('STEP AP214'),
    '1' );
FILE_NAME ('socket button head screw_iso_ISO 7380 - M4 x 8 - 8N.step',
    '2026-10-23T14:45:25',
    ( '' ),
    ( '' ),
    'SwSTEP 2.0',
    'SolidWorks 2026',
    '' );
FILE_SCHEMA (( 'AUTOMOTIVE_DESIGN' ));
ENDSEC;

DATA;
#5=CARTESIAN_POINT ( 'NONE',  ( 10.20000000000000107, 1.971681346627238735E-16, -1.610000000000000098 ) ) ;
#9=ORIENTED_EDGE ( 'NONE', *, *, #93, .F. ) ;
#11=VERTEX_POINT ( 'NONE', #3151 ) ;
#12=EDGE_LOOP ( 'NONE', ( #4243, #1543, #1314, #4388, #708 ) ) ;
#17=ORIENTED_EDGE ( 'NONE', *, *, #5283, .F. ) ;
#27=DIRECTION ( 'NONE',  ( 0.000000000000000000, 0.000000000000000000, -1.000000000000000000 ) ) ;
#60=DIRECTION ( 'NONE',  ( -0.7071067811865492381, 8.659560562354911904E-17, -0.7071067811865457964 ) ) ;
#64=ORIENTED_EDGE ( 'NONE', *, *, #3045, .T. ) ;
#73=VERTEX_POINT ( 'NONE', #3260 ) ;
#88=ADVANCED_FACE ( 'NONE', ( #5011, #2771 ), #1450, .T. ) ;
#93=EDGE_CURVE ( 'NONE', #5647, #11, #1098, .T. ) ;
#101=CARTESIAN_POINT ( 'NONE',  ( 0.000000000000000000, -0.7216878364870318308, -1.250000000000000000 ) ) ;
#107=DIRECTION ( 'NONE',  ( -0.000000000000000000, 0.000000000000000000, 1.000000000000000000 ) ) ;
#121=VECTOR ( 'NONE', #3967, 999.9999999999998863 ) ;
#124=ADVANCED_FACE ( 'NONE', ( #4956 ), #3318, .T. ) ;
#138=CIRCLE ( 'NONE', #1889, 1.999999999999999112 ) ;
#149=EDGE_CURVE ( 'NONE', #3887, #4410, #641, .T. ) ;
#151=DIRECTION ( 'NONE',  ( 0.000000000000000000, -0.4999999999999998890, 0.8660254037844387076 ) ) ;
#159=VECTOR ( 'NONE', #187, 1000.000000000000114 ) ;
#168=DIRECTION ( 'NONE',  ( -1.000000000000000000, -0.000000000000000000, -0.000000000000000000 ) ) ;
#179=ORIENTED_EDGE ( 'NONE', *, *, #1806, .T. ) ;
#187=DIRECTION ( 'NONE',  ( -0.000000000000000000, -0.5000000000000002220, 0.8660254037844384856 ) ) ;
#211=( GEOMETRIC_REPRESENTATION_CONTEXT ( 3 ) GLOBAL_UNCERTAINTY_ASSIGNED_CONTEXT ( ( #5230 ) ) GLOBAL_UNIT_ASSIGNED_CONTEXT ( ( #2989, #5121, #2439 ) ) REPRESENTATION_CONTEXT ( 'NONE', 'WORKASPACE' ) );
#212=DIRECTION ( 'NONE',  ( 0.000000000000000000, 0.000000000000000000, 1.000000000000000000 ) ) ;
#214=EDGE_LOOP ( 'NONE', ( #9, #1202, #2223 ) ) ;
#215=CARTESIAN_POINT ( 'NONE',  ( 1.300000000000000044, 0.7216878364870328300, -1.250000000000000000 ) ) ;
#223=LINE ( 'NONE', #741, #591 ) ;
#224=EDGE_CURVE ( 'NONE', #1931, #3723, #579, .T. ) ;
#227=ORIENTED_EDGE ( 'NONE', *, *, #1608, .T. ) ;
#234=DIRECTION ( 'NONE',  ( 0.000000000000000000, 0.000000000000000000, 1.000000000000000000 ) ) ;
#240=CARTESIAN_POINT ( 'NONE',  ( 1.820000000000000062, 3.799999999999999378, 0.000000000000000000 ) ) ;
#242=FACE_OUTER_BOUND ( 'NONE', #323, .T. ) ;
#252=CARTESIAN_POINT ( 'NONE',  ( 1.820000000000000062, 0.000000000000000000, 3.799999999999999378 ) ) ;
#257=EDGE_CURVE ( 'NONE', #4241, #4349, #3460, .T. ) ;
#260=CARTESIAN_POINT ( 'NONE',  ( 9.809999999999998721, 0.000000000000000000, 0.000000000000000000 ) ) ;
#270=DIRECTION ( 'NONE',  ( -0.000000000000000000, 0.000000000000000000, 1.000000000000000000 ) ) ;
#272=DIRECTION ( 'NONE',  ( 0.000000000000000000, 0.000000000000000000, 1.000000000000000000 ) ) ;
#283=CARTESIAN_POINT ( 'NONE',  ( 0.000000000000000000, 0.000000000000000000, 0.000000000000000000 ) ) ;
#286=VERTEX_POINT ( 'NONE', #2592 ) ;
#288=DIRECTION ( 'NONE',  ( 0.000000000000000000, 0.000000000000000000, 1.000000000000000000 ) ) ;
#309=AXIS2_PLACEMENT_3D ( 'NONE', #1717, #5231, #3017 ) ;
#319=EDGE_CURVE ( 'NONE', #2874, #3841, #1900, .T. ) ;
#323=EDGE_LOOP ( 'NONE', ( #4810, #3958, #689, #578, #1562 ) ) ;
#330=AXIS2_PLACEMENT_3D ( 'NONE', #260, #4634, #2330 ) ;
#331=VECTOR ( 'NONE', #2830, 1000.000000000000114 ) ;
#337=MECHANICAL_DESIGN_GEOMETRIC_PRESENTATION_REPRESENTATION('',(#5488),#5215);
#345=CIRCLE ( 'NONE', #3293, 1.249999999999999778 ) ;
#349=DIRECTION ( 'NONE',  ( 0.000000000000000000, 0.000000000000000000, 1.000000000000000000 ) ) ;
#350=CARTESIAN_POINT ( 'NONE',  ( 1.300000000000000044, -1.082531754730548412, 0.6249999999999998890 ) ) ;
#360=CARTESIAN_POINT ( 'NONE',  ( 10.20000000000000107, 0.000000000000000000, 0.000000000000000000 ) ) ;
#371=CARTESIAN_POINT ( 'NONE',  ( 2.200000000000000178, 0.000000000000000000, 3.799999999999999378 ) ) ;
#380=DIRECTION ( 'NONE',  ( 0.000000000000000000, 0.000000000000000000, 1.000000000000000000 ) ) ;
#383=ADVANCED_FACE ( 'NONE', ( #753 ), #4691, .T. ) ;
#385=LINE ( 'NONE', #4762, #4365 ) ;
#408=ORIENTED_EDGE ( 'NONE', *, *, #937, .F. ) ;
#421=CARTESIAN_POINT ( 'NONE',  ( -997.9783121635130101, 0.000000000000000000, 0.000000000000000000 ) ) ;
#422=CONICAL_SURFACE ( 'NONE', #2718, 1.610000000000000098, 0.7853981633974458365 ) ;
#430=DIRECTION ( 'NONE',  ( -1.000000000000000000, -0.000000000000000000, -0.000000000000000000 ) ) ;
#441=DIRECTION ( 'NONE',  ( 0.000000000000000000, 0.000000000000000000, 1.000000000000000000 ) ) ;
#446=EDGE_CURVE ( 'NONE', #5376, #2874, #4836, .T. ) ;
#457=FACE_OUTER_BOUND ( 'NONE', #2345, .T. ) ;
#460=ORIENTED_EDGE ( 'NONE', *, *, #4224, .T. ) ;
#466=ORIENTED_EDGE ( 'NONE', *, *, #2118, .T. ) ;
#477=STYLED_ITEM ( 'NONE', ( #1639 ), #622 ) ;
#492=ORIENTED_EDGE ( 'NONE', *, *, #2197, .F. ) ;
#501=EDGE_LOOP ( 'NONE', ( #1369, #4531 ) ) ;
#515=AXIS2_PLACEMENT_3D ( 'NONE', #5037, #699, #4209 ) ;
#517=EDGE_CURVE ( 'NONE', #3462, #3841, #3089, .T. ) ;
#543=LINE ( 'NONE', #4401, #4361 ) ;
#552=ORIENTED_EDGE ( 'NONE', *, *, #1022, .F. ) ;
#557=ORIENTED_EDGE ( 'NONE', *, *, #149, .F. ) ;
#578=ORIENTED_EDGE ( 'NONE', *, *, #2981, .F. ) ;
#579=LINE ( 'NONE', #2332, #2349 ) ;
#582=AXIS2_PLACEMENT_3D ( 'NONE', #3488, #2656, #3891 ) ;
#591=VECTOR ( 'NONE', #721, 999.9999999999998863 ) ;
#597=CARTESIAN_POINT ( 'NONE',  ( 1.300000000000000044, 0.000000000000000000, 0.000000000000000000 ) ) ;
#598=EDGE_CURVE ( 'NONE', #4504, #73, #1734, .T. ) ;
#601=AXIS2_PLACEMENT_3D ( 'NONE', #4698, #1222, #441 ) ;
#604=DIRECTION ( 'NONE',  ( -1.000000000000000000, -0.000000000000000000, -0.000000000000000000 ) ) ;
#605=( NAMED_UNIT ( * ) SI_UNIT ( $, .STERADIAN. ) SOLID_ANGLE_UNIT ( ) );
#608=LINE ( 'NONE', #5502, #3645 ) ;
#609=ORIENTED_EDGE ( 'NONE', *, *, #5454, .T. ) ;
#610=DIRECTION ( 'NONE',  ( -1.000000000000000000, 0.000000000000000000, 0.000000000000000000 ) ) ;
#619=AXIS2_PLACEMENT_3D ( 'NONE', #3226, #1030, #1523 ) ;
#622=ADVANCED_BREP_SHAPE_REPRESENTATION ( '', ( #698, #1336 ), #5443 ) ;
#632=ORIENTED_EDGE ( 'NONE', *, *, #3010, .T. ) ;
#634=DIRECTION ( 'NONE',  ( 0.000000000000000000, -0.8660254037844385966, 0.5000000000000001110 ) ) ;
#641=LINE ( 'NONE', #3712, #1066 ) ;
#648=ORIENTED_EDGE ( 'NONE', *, *, #866, .T. ) ;
#649=CYLINDRICAL_SURFACE ( 'NONE', #3107, 1.999999999999999112 ) ;
#657=DIRECTION ( 'NONE',  ( 0.000000000000000000, 0.000000000000000000, 1.000000000000000000 ) ) ;
#664=CARTESIAN_POINT ( 'NONE',  ( 1.300000000000000044, -1.443375672974063884, -3.691112476943992763E-18 ) ) ;
#676=CARTESIAN_POINT ( 'NONE',  ( 1.300000000000000044, 0.7216878364870328300, 1.249999999999999778 ) ) ;
#681=AXIS2_PLACEMENT_3D ( 'NONE', #5350, #27, #3508 ) ;
#689=ORIENTED_EDGE ( 'NONE', *, *, #1022, .T. ) ;
#691=VECTOR ( 'NONE', #3676, 1000.000000000000000 ) ;
#696=AXIS2_PLACEMENT_3D ( 'NONE', #2101, #4689, #3000 ) ;
#698=MANIFOLD_SOLID_BREP ( 'Hex', #3733 ) ;
#699=DIRECTION ( 'NONE',  ( -1.000000000000000000, -0.000000000000000000, -0.000000000000000000 ) ) ;
#700=EDGE_LOOP ( 'NONE', ( #2599, #2976, #1076 ) ) ;
#703=CARTESIAN_POINT ( 'NONE',  ( 1.300000000000000044, -0.7216878364870318308, 1.249999999999999778 ) ) ;
#708=ORIENTED_EDGE ( 'NONE', *, *, #2114, .T. ) ;
#712=CARTESIAN_POINT ( 'NONE',  ( 2.400000000000000799, 0.000000000000000000, 0.000000000000000000 ) ) ;
#718=ORIENTED_EDGE ( 'NONE', *, *, #1122, .F. ) ;
#721=DIRECTION ( 'NONE',  ( -0.000000000000000000, -0.4999999999999999445, -0.8660254037844387076 ) ) ;
#727=DIRECTION ( 'NONE',  ( 0.000000000000000000, 0.000000000000000000, -1.000000000000000000 ) ) ;
#728=DIRECTION ( 'NONE',  ( 1.000000000000000000, 0.000000000000000000, 0.000000000000000000 ) ) ;
#735=CARTESIAN_POINT ( 'NONE',  ( 0.000000000000000000, 1.443375672974065216, 7.017607234860990640E-28 ) ) ;
#741=CARTESIAN_POINT ( 'NONE',  ( 0.000000000000000000, -1.443375672974063884, -3.691112476943992763E-18 ) ) ;
#742=( NAMED_UNIT ( * ) PLANE_ANGLE_UNIT ( ) SI_UNIT ( $, .RADIAN. ) );
#753=FACE_OUTER_BOUND ( 'NONE', #4274, .T. ) ;
#761=LINE ( 'NONE', #5191, #3103 ) ;
#778=DIRECTION ( 'NONE',  ( 0.000000000000000000, 0.000000000000000000, 1.000000000000000000 ) ) ;
#780=ORIENTED_EDGE ( 'NONE', *, *, #5104, .F. ) ;
#786=ORIENTED_EDGE ( 'NONE', *, *, #5454, .F. ) ;
#787=FACE_OUTER_BOUND ( 'NONE', #1791, .T. ) ;
#797=ORIENTED_EDGE ( 'NONE', *, *, #598, .T. ) ;
#800=EDGE_CURVE ( 'NONE', #3462, #2713, #891, .T. ) ;
#802=AXIS2_PLACEMENT_3D ( 'NONE', #5681, #2572, #3811 ) ;
#813=DIRECTION ( 'NONE',  ( -1.000000000000000000, -0.000000000000000000, -0.000000000000000000 ) ) ;
#816=ORIENTED_EDGE ( 'NONE', *, *, #4686, .T. ) ;
#823=CARTESIAN_POINT ( 'NONE',  ( 0.000000000000000000, -1.443375672974063884, -3.691112476943992763E-18 ) ) ;
#838=DIRECTION ( 'NONE',  ( -1.000000000000000000, -0.000000000000000000, -0.000000000000000000 ) ) ;
#850=ADVANCED_FACE ( 'NONE', ( #3269 ), #1545, .T. ) ;
#853=ADVANCED_FACE ( 'NONE', ( #242 ), #4133, .T. ) ;
#866=EDGE_CURVE ( 'NONE', #1059, #4467, #5111, .T. ) ;
#891=CIRCLE ( 'NONE', #1633, 3.799999999999999378 ) ;
#910=ADVANCED_FACE ( 'NONE', ( #5075 ), #4936, .F. ) ;
#917=CARTESIAN_POINT ( 'NONE',  ( 0.000000000000000000, -0.7216878364870318308, -1.250000000000000000 ) ) ;
#928=VERTEX_POINT ( 'NONE', #2463 ) ;
#937=EDGE_CURVE ( 'NONE', #2377, #1307, #3355, .T. ) ;
#940=ORIENTED_EDGE ( 'NONE', *, *, #5169, .F. ) ;
#951=EDGE_CURVE ( 'NONE', #3918, #1059, #3724, .T. ) ;
#956=EDGE_LOOP ( 'NONE', ( #1164, #1024 ) ) ;
#962=ADVANCED_FACE ( 'NONE', ( #5049 ), #649, .T. ) ;
#975=EDGE_CURVE ( 'NONE', #2597, #4467, #4617, .T. ) ;
#981=VECTOR ( 'NONE', #2742, 1000.000000000000000 ) ;
#987=ORIENTED_EDGE ( 'NONE', *, *, #1553, .F. ) ;
#995=DIRECTION ( 'NONE',  ( -1.000000000000000000, -0.000000000000000000, -0.000000000000000000 ) ) ;
#1022=EDGE_CURVE ( 'NONE', #3723, #3918, #761, .T. ) ;
#1024=ORIENTED_EDGE ( 'NONE', *, *, #1343, .T. ) ;
#1026=FACE_OUTER_BOUND ( 'NONE', #3874, .T. ) ;
#1030=DIRECTION ( 'NONE',  ( 0.000000000000000000, 0.000000000000000000, 1.000000000000000000 ) ) ;
#1037=DIRECTION ( 'NONE',  ( 0.000000000000000000, 0.8660254037844387076, 0.4999999999999998890 ) ) ;
#1049=CIRCLE ( 'NONE', #5651, 2.199999999999999289 ) ;
#1059=VERTEX_POINT ( 'NONE', #735 ) ;
#1061=PLANE ( 'NONE',  #3472 ) ;
#1066=VECTOR ( 'NONE', #610, 1000.000000000000000 ) ;
#1067=CARTESIAN_POINT ( 'NONE',  ( 2.200000000000000178, 4.653657836759941744E-16, -3.799999999999999378 ) ) ;
#1072=CIRCLE ( 'NONE', #5025, 0.2000000000000000944 ) ;
#1075=CARTESIAN_POINT ( 'NONE',  ( 2.200000000000000622, 1.999999999999999112, 0.000000000000000000 ) ) ;
#1076=ORIENTED_EDGE ( 'NONE', *, *, #2114, .F. ) ;
#1077=DIRECTION ( 'NONE',  ( 0.000000000000000000, 0.000000000000000000, 1.000000000000000000 ) ) ;
#1078=LINE ( 'NONE', #101, #1548 ) ;
#1082=ORIENTED_EDGE ( 'NONE', *, *, #4109, .F. ) ;
#1085=CARTESIAN_POINT ( 'NONE',  ( 10.20000000000000107, 0.000000000000000000, 0.000000000000000000 ) ) ;
#1086=( LENGTH_UNIT ( ) NAMED_UNIT ( * ) SI_UNIT ( .MILLI., .METRE. ) );
#1088=ORIENTED_EDGE ( 'NONE', *, *, #2306, .T. ) ;
#1093=DIRECTION ( 'NONE',  ( -0.5000000000000044409, 0.000000000000000000, 0.8660254037844360431 ) ) ;
#1096=DIRECTION ( 'NONE',  ( -0.000000000000000000, 0.5000000000000001110, 0.8660254037844385966 ) ) ;
#1098=LINE ( 'NONE', #2881, #331 ) ;
#1104=ORIENTED_EDGE ( 'NONE', *, *, #517, .F. ) ;
#1107=CARTESIAN_POINT ( 'NONE',  ( 0.000000000000000000, 0.000000000000000000, 0.000000000000000000 ) ) ;
#1122=EDGE_CURVE ( 'NONE', #5494, #928, #1072, .T. ) ;
#1126=CYLINDRICAL_SURFACE ( 'NONE', #1978, 3.799999999999999378 ) ;
#1133=CARTESIAN_POINT ( 'NONE',  ( 0.000000000000000000, 0.7216878364870328300, 1.249999999999999778 ) ) ;
#1149=EDGE_CURVE ( 'NONE', #2807, #1307, #2547, .T. ) ;
#1156=VECTOR ( 'NONE', #2540, 999.9999999999998863 ) ;
#1163=CARTESIAN_POINT ( 'NONE',  ( 1.300000000000000044, -1.443375672974063884, -3.691112476943992763E-18 ) ) ;
#1164=ORIENTED_EDGE ( 'NONE', *, *, #5104, .T. ) ;
#1167=DIRECTION ( 'NONE',  ( -0.000000000000000000, 0.5000000000000001110, 0.8660254037844385966 ) ) ;
#1170=AXIS2_PLACEMENT_3D ( 'NONE', #4296, #838, #1701 ) ;
#1176=VECTOR ( 'NONE', #5436, 1000.000000000000000 ) ;
#1177=EDGE_CURVE ( 'NONE', #1387, #5593, #1996, .T. ) ;
#1186=LINE ( 'NONE', #2075, #2523 ) ;
#1197=ORIENTED_EDGE ( 'NONE', *, *, #4090, .F. ) ;
#1202=ORIENTED_EDGE ( 'NONE', *, *, #3045, .F. ) ;
#1205=DIRECTION ( 'NONE',  ( -1.000000000000000000, -0.000000000000000000, -0.000000000000000000 ) ) ;
#1206=FILL_AREA_STYLE_COLOUR ( '', #3512 ) ;
#1213=CARTESIAN_POINT ( 'NONE',  ( 10.20000000000000107, 0.000000000000000000, 1.610000000000000098 ) ) ;
#1214=DIRECTION ( 'NONE',  ( 0.000000000000000000, -0.8660254037844385966, -0.5000000000000003331 ) ) ;
#1216=DIRECTION ( 'NONE',  ( -1.000000000000000000, -0.000000000000000000, -0.000000000000000000 ) ) ;
#1222=DIRECTION ( 'NONE',  ( -1.000000000000000000, -0.000000000000000000, -0.000000000000000000 ) ) ;
#1224=DIRECTION ( 'NONE',  ( -1.000000000000000000, 0.000000000000000000, 0.000000000000000000 ) ) ;
#1237=CIRCLE ( 'NONE', #1785, 1.249999999999999778 ) ;
#1238=CARTESIAN_POINT ( 'NONE',  ( 2.200000000000000178, 0.000000000000000000, 0.000000000000000000 ) ) ;
#1248=EDGE_LOOP ( 'NONE', ( #492, #1082, #2541 ) ) ;
#1255=UNCERTAINTY_MEASURE_WITH_UNIT (LENGTH_MEASURE( 1.000000000000000082E-05 ), #1086, 'distance_accuracy_value', 'NONE');
#1258=ORIENTED_EDGE ( 'NONE', *, *, #951, .F. ) ;
#1281=EDGE_LOOP ( 'NONE', ( #408, #5167, #940 ) ) ;
#1302=EDGE_LOOP ( 'NONE', ( #5567, #2968, #2486, #718 ) ) ;
#1307=VERTEX_POINT ( 'NONE', #5326 ) ;
#1314=ORIENTED_EDGE ( 'NONE', *, *, #1149, .T. ) ;
#1327=CARTESIAN_POINT ( 'NONE',  ( 0.000000000000000000, 4.653657836759941744E-16, -3.799999999999999378 ) ) ;
#1331=ORIENTED_EDGE ( 'NONE', *, *, #446, .T. ) ;
#1336=AXIS2_PLACEMENT_3D ( 'NONE', #283, #2997, #5213 ) ;
#1343=EDGE_CURVE ( 'NONE', #1387, #5494, #5221, .T. ) ;
#1360=EDGE_LOOP ( 'NONE', ( #1473, #179, #5383, #3317 ) ) ;
#1362=SHAPE_REPRESENTATION ( 'socket button head screw_iso_ISO 7380 - M4 x 8 - 8N', ( #1336 ), #5443 ) ;
#1365=PLANE ( 'NONE',  #1599 ) ;
#1369=ORIENTED_EDGE ( 'NONE', *, *, #3787, .F. ) ;
#1387=VERTEX_POINT ( 'NONE', #2705 ) ;
#1391=EDGE_LOOP ( 'NONE', ( #1710, #4167, #3755, #5672, #2782 ) ) ;
#1399=DIRECTION ( 'NONE',  ( -0.000000000000000000, 0.4999999999999998890, -0.8660254037844387076 ) ) ;
#1443=AXIS2_PLACEMENT_3D ( 'NONE', #4550, #4182, #234 ) ;
#1448=CARTESIAN_POINT ( 'NONE',  ( 1.300000000000000044, 0.000000000000000000, 0.000000000000000000 ) ) ;
#1449=VERTEX_POINT ( 'NONE', #4429 ) ;
#1450=PLANE ( 'NONE',  #2788 ) ;
#1462=VERTEX_POINT ( 'NONE', #3572 ) ;
#1473=ORIENTED_EDGE ( 'NONE', *, *, #3717, .T. ) ;
#1480=ORIENTED_EDGE ( 'NONE', *, *, #3678, .F. ) ;
#1481=DIRECTION ( 'NONE',  ( -1.000000000000000000, 0.000000000000000000, 0.000000000000000000 ) ) ;
#1493=LINE ( 'NONE', #3742, #4639 ) ;
#1503=FACE_BOUND ( 'NONE', #956, .T. ) ;
#1517=CARTESIAN_POINT ( 'NONE',  ( 1.300000000000000044, 1.443375672974065216, 7.017607234860990640E-28 ) ) ;
#1523=DIRECTION ( 'NONE',  ( 1.000000000000000000, 0.000000000000000000, 0.000000000000000000 ) ) ;
#1526=CONICAL_SURFACE ( 'NONE', #1895, 1.610000000000000098, 0.7853981633974458365 ) ;
#1532=CARTESIAN_POINT ( 'NONE',  ( 1.300000000000000044, -0.7216878364870318308, -1.250000000000000000 ) ) ;
#1543=ORIENTED_EDGE ( 'NONE', *, *, #5588, .T. ) ;
#1545=PLANE ( 'NONE',  #5581 ) ;
#1548=VECTOR ( 'NONE', #1399, 1000.000000000000114 ) ;
#1553=EDGE_CURVE ( 'NONE', #2807, #3887, #3203, .T. ) ;
#1562=ORIENTED_EDGE ( 'NONE', *, *, #4062, .F. ) ;
#1564=DIRECTION ( 'NONE',  ( -1.000000000000000000, -0.000000000000000000, -0.000000000000000000 ) ) ;
#1567=CARTESIAN_POINT ( 'NONE',  ( 8.673617379884035472E-16, -1.899999999999999689, -3.490243377569955075E-16 ) ) ;
#1587=CARTESIAN_POINT ( 'NONE',  ( 1.300000000000000044, -0.7216878364870318308, 1.249999999999999778 ) ) ;
#1593=DIRECTION ( 'NONE',  ( -1.000000000000000000, 0.000000000000000000, -0.000000000000000000 ) ) ;
#1599=AXIS2_PLACEMENT_3D ( 'NONE', #2196, #1676, #3121 ) ;
#1608=EDGE_CURVE ( 'NONE', #2874, #4349, #5402, .T. ) ;
#1609=VECTOR ( 'NONE', #2079, 1000.000000000000000 ) ;
#1623=CIRCLE ( 'NONE', #5571, 3.799999999999999378 ) ;
#1627=ORIENTED_EDGE ( 'NONE', *, *, #5109, .F. ) ;
#1633=AXIS2_PLACEMENT_3D ( 'NONE', #1926, #3682, #4060 ) ;
#1637=AXIS2_PLACEMENT_3D ( 'NONE', #3172, #5352, #3944 ) ;
#1639=PRESENTATION_STYLE_ASSIGNMENT (( #3822 ) ) ;
#1645=CARTESIAN_POINT ( 'NONE',  ( 1.300000000000000044, -0.7216878364870319418, 1.249999999999999778 ) ) ;
#1653=ORIENTED_EDGE ( 'NONE', *, *, #2134, .F. ) ;
#1665=CARTESIAN_POINT ( 'NONE',  ( 1.820000000000000062, 0.000000000000000000, 0.000000000000000000 ) ) ;
#1667=EDGE_CURVE ( 'NONE', #2953, #5376, #2003, .T. ) ;
#1674=LINE ( 'NONE', #3889, #3633 ) ;
#1676=DIRECTION ( 'NONE',  ( -1.000000000000000000, 0.000000000000000000, 0.000000000000000000 ) ) ;
#1677=ORIENTED_EDGE ( 'NONE', *, *, #5109, .T. ) ;
#1689=( NAMED_UNIT ( * ) SI_UNIT ( $, .STERADIAN. ) SOLID_ANGLE_UNIT ( ) );
#1693=CONICAL_SURFACE ( 'NONE', #2984, 1732.050807568856271, 1.047197551196592524 ) ;
#1699=DIRECTION ( 'NONE',  ( -1.000000000000000000, 0.000000000000000000, 0.000000000000000000 ) ) ;
#1701=DIRECTION ( 'NONE',  ( 0.000000000000000000, 0.000000000000000000, 1.000000000000000000 ) ) ;
#1705=ADVANCED_FACE ( 'NONE', ( #5001 ), #1061, .T. ) ;
#1710=ORIENTED_EDGE ( 'NONE', *, *, #319, .T. ) ;
#1717=CARTESIAN_POINT ( 'NONE',  ( 8.673617379884035472E-16, 0.000000000000000000, 0.000000000000000000 ) ) ;
#1734=LINE ( 'NONE', #5, #4383 ) ;
#1736=ORIENTED_EDGE ( 'NONE', *, *, #937, .T. ) ;
#1737=DIRECTION ( 'NONE',  ( -1.000000000000000000, -0.000000000000000000, -0.000000000000000000 ) ) ;
#1742=FACE_OUTER_BOUND ( 'NONE', #1302, .T. ) ;
#1758=CARTESIAN_POINT ( 'NONE',  ( 4.336808689942017736E-16, -0.7216878364870318308, 1.249999999999999778 ) ) ;
#1759=EDGE_LOOP ( 'NONE', ( #3032, #3001 ) ) ;
#1785=AXIS2_PLACEMENT_3D ( 'NONE', #597, #4169, #1921 ) ;
#1791=EDGE_LOOP ( 'NONE', ( #816, #797, #1799, #4616 ) ) ;
#1797=DIRECTION ( 'NONE',  ( -1.000000000000000000, -0.000000000000000000, -0.000000000000000000 ) ) ;
#1799=ORIENTED_EDGE ( 'NONE', *, *, #3717, .F. ) ;
#1806=EDGE_CURVE ( 'NONE', #73, #5593, #2472, .T. ) ;
#1817=EDGE_CURVE ( 'NONE', #3841, #2953, #3201, .T. ) ;
#1830=DIRECTION ( 'NONE',  ( 0.000000000000000000, 0.000000000000000000, 1.000000000000000000 ) ) ;
#1838=DIRECTION ( 'NONE',  ( 0.000000000000000000, 0.000000000000000000, 1.000000000000000000 ) ) ;
#1839=DIRECTION ( 'NONE',  ( -1.000000000000000000, 0.000000000000000000, 0.000000000000000000 ) ) ;
#1876=ORIENTED_EDGE ( 'NONE', *, *, #951, .T. ) ;
#1884=ORIENTED_EDGE ( 'NONE', *, *, #1177, .F. ) ;
#1889=AXIS2_PLACEMENT_3D ( 'NONE', #4666, #728, #5559 ) ;
#1892=AXIS2_PLACEMENT_3D ( 'NONE', #1075, #1593, #270 ) ;
#1894=CARTESIAN_POINT ( 'NONE',  ( 0.000000000000000000, 0.000000000000000000, 1.999999999999999112 ) ) ;
#1895=AXIS2_PLACEMENT_3D ( 'NONE', #1905, #4149, #1930 ) ;
#1900=CIRCLE ( 'NONE', #1170, 3.799999999999999378 ) ;
#1905=CARTESIAN_POINT ( 'NONE',  ( 10.20000000000000107, 0.000000000000000000, 0.000000000000000000 ) ) ;
#1916=CARTESIAN_POINT ( 'NONE',  ( 0.000000000000000000, -0.7216878364870318308, 1.249999999999999778 ) ) ;
#1921=DIRECTION ( 'NONE',  ( 0.000000000000000000, 0.000000000000000000, 1.000000000000000000 ) ) ;
#1923=ORIENTED_EDGE ( 'NONE', *, *, #4062, .T. ) ;
#1926=CARTESIAN_POINT ( 'NONE',  ( 2.200000000000000178, 0.000000000000000000, 0.000000000000000000 ) ) ;
#1930=DIRECTION ( 'NONE',  ( 0.000000000000000000, 0.000000000000000000, 1.000000000000000000 ) ) ;
#1931=VERTEX_POINT ( 'NONE', #2208 ) ;
#1940=CARTESIAN_POINT ( 'NONE',  ( 0.000000000000000000, 1.443375672974065216, 7.017607234860990640E-28 ) ) ;
#1949=MECHANICAL_DESIGN_GEOMETRIC_PRESENTATION_REPRESENTATION('',(#477),#211);
#1965=EDGE_LOOP ( 'NONE', ( #5434, #2059, #2085, #4112, #786 ) ) ;
#1966=PRODUCT_DEFINITION_SHAPE ( 'NONE', 'NONE',  #3839 ) ;
#1969=DIRECTION ( 'NONE',  ( 0.000000000000000000, 0.000000000000000000, 1.000000000000000000 ) ) ;
#1978=AXIS2_PLACEMENT_3D ( 'NONE', #4237, #1564, #288 ) ;
#1983=VERTEX_POINT ( 'NONE', #3960 ) ;
#1996=CIRCLE ( 'NONE', #802, 0.2000000000000000944 ) ;
#2003=CIRCLE ( 'NONE', #2091, 3.799999999999999378 ) ;
#2008=ADVANCED_FACE ( 'NONE', ( #4447 ), #3021, .F. ) ;
#2026=ORIENTED_EDGE ( 'NONE', *, *, #1817, .F. ) ;
#2027=CARTESIAN_POINT ( 'NONE',  ( 0.000000000000000000, 0.7216878364870328300, -1.250000000000000000 ) ) ;
#2041=DIRECTION ( 'NONE',  ( -0.7071067811865492381, 0.000000000000000000, 0.7071067811865457964 ) ) ;
#2051=CARTESIAN_POINT ( 'NONE',  ( 1.300000000000000044, -0.7216878364870318308, -1.250000000000000000 ) ) ;
#2059=ORIENTED_EDGE ( 'NONE', *, *, #517, .T. ) ;
#2061=ADVANCED_FACE ( 'NONE', ( #3614 ), #5370, .T. ) ;
#2062=PRODUCT ( 'socket button head screw_iso_ISO 7380 - M4 x 8 - 8N', 'socket button head screw_iso_ISO 7380 - M4 x 8 - 8N', '', ( #3024 ) ) ;
#2071=APPLICATION_CONTEXT ( 'automotive_design' ) ;
#2075=CARTESIAN_POINT ( 'NONE',  ( 2.021687836487040535, 2.655529440325959183E-32, -2.168404344971008868E-16 ) ) ;
#2079=DIRECTION ( 'NONE',  ( -0.000000000000000000, -1.000000000000000000, -0.000000000000000000 ) ) ;
#2085=ORIENTED_EDGE ( 'NONE', *, *, #319, .F. ) ;
#2091=AXIS2_PLACEMENT_3D ( 'NONE', #4545, #604, #5497 ) ;
#2101=CARTESIAN_POINT ( 'NONE',  ( 1.300000000000000044, -0.7216878364870319418, 1.249999999999999778 ) ) ;
#2110=EDGE_LOOP ( 'NONE', ( #466, #3095, #3192, #3945, #1876, #648 ) ) ;
#2111=DIRECTION ( 'NONE',  ( 0.000000000000000000, -1.000000000000000000, 0.000000000000000000 ) ) ;
#2114=EDGE_CURVE ( 'NONE', #1462, #1931, #345, .T. ) ;
#2118=EDGE_CURVE ( 'NONE', #4467, #4410, #4907, .T. ) ;
#2130=PLANE ( 'NONE',  #696 ) ;
#2134=EDGE_CURVE ( 'NONE', #4643, #4872, #1078, .T. ) ;
#2137=FACE_OUTER_BOUND ( 'NONE', #214, .T. ) ;
#2139=FACE_OUTER_BOUND ( 'NONE', #2563, .T. ) ;
#2141=CARTESIAN_POINT ( 'NONE',  ( 2.400000000000000799, 0.000000000000000000, 2.199999999999999289 ) ) ;
#2180=DIRECTION ( 'NONE',  ( -1.000000000000000000, -0.000000000000000000, -0.000000000000000000 ) ) ;
#2189=DIRECTION ( 'NONE',  ( 0.000000000000000000, 0.000000000000000000, 1.000000000000000000 ) ) ;
#2196=CARTESIAN_POINT ( 'NONE',  ( 1.300000000000000044, -0.7216878364870319418, 1.249999999999999778 ) ) ;
#2197=EDGE_CURVE ( 'NONE', #2597, #2807, #5067, .T. ) ;
#2208=CARTESIAN_POINT ( 'NONE',  ( 1.300000000000000044, 0.000000000000000000, -1.250000000000000000 ) ) ;
#2216=SPHERICAL_SURFACE ( 'NONE', #681, 4.324969328314201888 ) ;
#2223=ORIENTED_EDGE ( 'NONE', *, *, #2442, .F. ) ;
#2235=ADVANCED_FACE ( 'NONE', ( #4152 ), #1126, .T. ) ;
#2286=CARTESIAN_POINT ( 'NONE',  ( 1.300000000000000044, -0.7216878364870319418, 1.249999999999999778 ) ) ;
#2306=EDGE_CURVE ( 'NONE', #928, #5593, #138, .T. ) ;
#2312=ORIENTED_EDGE ( 'NONE', *, *, #4232, .F. ) ;
#2321=CARTESIAN_POINT ( 'NONE',  ( 10.20000000000000107, 0.000000000000000000, 0.000000000000000000 ) ) ;
#2329=AXIS2_PLACEMENT_3D ( 'NONE', #360, #1797, #2664 ) ;
#2330=DIRECTION ( 'NONE',  ( 0.000000000000000000, 0.000000000000000000, 1.000000000000000000 ) ) ;
#2332=CARTESIAN_POINT ( 'NONE',  ( 1.300000000000000044, 0.7216878364870328300, -1.250000000000000000 ) ) ;
#2345=EDGE_LOOP ( 'NONE', ( #1480, #3288, #1331, #227, #3686 ) ) ;
#2349=VECTOR ( 'NONE', #4098, 1000.000000000000000 ) ;
#2356=( LENGTH_UNIT ( ) NAMED_UNIT ( * ) SI_UNIT ( .MILLI., .METRE. ) );
#2357=VECTOR ( 'NONE', #1167, 1000.000000000000000 ) ;
#2362=ORIENTED_EDGE ( 'NONE', *, *, #3391, .T. ) ;
#2377=VERTEX_POINT ( 'NONE', #2732 ) ;
#2380=CARTESIAN_POINT ( 'NONE',  ( 9.809999999999998721, 0.000000000000000000, 1.999999999999999556 ) ) ;
#2385=DIRECTION ( 'NONE',  ( 0.000000000000000000, -0.5000000000000001110, -0.8660254037844385966 ) ) ;
#2389=EDGE_CURVE ( 'NONE', #3723, #1462, #1674, .T. ) ;
#2390=DIRECTION ( 'NONE',  ( 0.000000000000000000, 1.000000000000000000, 1.224646799147353207E-16 ) ) ;
#2401=DIRECTION ( 'NONE',  ( -1.000000000000000000, -0.000000000000000000, -0.000000000000000000 ) ) ;
#2429=CARTESIAN_POINT ( 'NONE',  ( 1.300000000000000044, -0.7216878364870319418, 1.249999999999999778 ) ) ;
#2430=AXIS2_PLACEMENT_3D ( 'NONE', #3981, #3439, #5197 ) ;
#2433=AXIS2_PLACEMENT_3D ( 'NONE', #5119, #3418, #5085 ) ;
#2439=( NAMED_UNIT ( * ) SI_UNIT ( $, .STERADIAN. ) SOLID_ANGLE_UNIT ( ) );
#2442=EDGE_CURVE ( 'NONE', #11, #2508, #4456, .T. ) ;
#2456=VECTOR ( 'NONE', #3756, 1000.000000000000114 ) ;
#2463=CARTESIAN_POINT ( 'NONE',  ( 2.400000000000000799, 0.000000000000000000, 1.999999999999999112 ) ) ;
#2470=SURFACE_STYLE_FILL_AREA ( #5203 ) ;
#2472=LINE ( 'NONE', #4205, #5311 ) ;
#2486=ORIENTED_EDGE ( 'NONE', *, *, #2306, .F. ) ;
#2487=DIRECTION ( 'NONE',  ( -0.000000000000000000, 0.4999999999999998890, -0.8660254037844387076 ) ) ;
#2508=VERTEX_POINT ( 'NONE', #350 ) ;
#2511=CARTESIAN_POINT ( 'NONE',  ( 1.300000000000000044, 0.000000000000000000, 0.000000000000000000 ) ) ;
#2514=CIRCLE ( 'NONE', #5369, 1.249999999999999778 ) ;
#2523=VECTOR ( 'NONE', #4234, 1000.000000000000114 ) ;
#2530=LINE ( 'NONE', #1213, #4738 ) ;
#2534=CARTESIAN_POINT ( 'NONE',  ( 1.300000000000000044, 0.000000000000000000, 0.000000000000000000 ) ) ;
#2538=FACE_OUTER_BOUND ( 'NONE', #3489, .T. ) ;
#2540=DIRECTION ( 'NONE',  ( -0.000000000000000000, -0.4999999999999999445, -0.8660254037844387076 ) ) ;
#2541=ORIENTED_EDGE ( 'NONE', *, *, #1149, .F. ) ;
#2547=CIRCLE ( 'NONE', #4016, 1.249999999999999778 ) ;
#2553=AXIS2_PLACEMENT_3D ( 'NONE', #2286, #5021, #4506 ) ;
#2562=CARTESIAN_POINT ( 'NONE',  ( 1.300000000000000044, -0.7216878364870319418, 1.249999999999999778 ) ) ;
#2563=EDGE_LOOP ( 'NONE', ( #3144, #4724, #5059, #1088 ) ) ;
#2572=DIRECTION ( 'NONE',  ( -0.000000000000000000, 1.000000000000000000, 1.224646799147353207E-16 ) ) ;
#2589=DIRECTION ( 'NONE',  ( 0.000000000000000000, 0.000000000000000000, 1.000000000000000000 ) ) ;
#2590=CARTESIAN_POINT ( 'NONE',  ( 1.300000000000000044, 0.7216878364870328300, 1.249999999999999778 ) ) ;
#2592=CARTESIAN_POINT ( 'NONE',  ( 2.021687836487040535, 2.168404344971008868E-16, 0.000000000000000000 ) ) ;
#2597=VERTEX_POINT ( 'NONE', #2937 ) ;
#2599=ORIENTED_EDGE ( 'NONE', *, *, #2389, .F. ) ;
#2616=ADVANCED_FACE ( 'NONE', ( #3375 ), #5129, .T. ) ;
#2618=ADVANCED_FACE ( 'NONE', ( #4322 ), #2130, .T. ) ;
#2622=AXIS2_PLACEMENT_3D ( 'NONE', #5413, #4123, #4605 ) ;
#2646=EDGE_CURVE ( 'NONE', #286, #1931, #1186, .T. ) ;
#2650=LINE ( 'NONE', #5243, #121 ) ;
#2656=DIRECTION ( 'NONE',  ( 0.000000000000000000, 0.8660254037844387076, -0.4999999999999999445 ) ) ;
#2662=APPLICATION_CONTEXT ( 'automotive_design' ) ;
#2664=DIRECTION ( 'NONE',  ( 0.000000000000000000, 0.000000000000000000, 1.000000000000000000 ) ) ;
#2681=DIRECTION ( 'NONE',  ( -1.000000000000000000, -0.000000000000000000, -0.000000000000000000 ) ) ;
#2705=CARTESIAN_POINT ( 'NONE',  ( 2.200000000000000622, 2.694222958124176020E-16, -2.199999999999999289 ) ) ;
#2713=VERTEX_POINT ( 'NONE', #371 ) ;
#2718=AXIS2_PLACEMENT_3D ( 'NONE', #4783, #1737, #5161 ) ;
#2732=CARTESIAN_POINT ( 'NONE',  ( 1.300000000000000044, 1.443375672974065216, 7.017607234860990640E-28 ) ) ;
#2742=DIRECTION ( 'NONE',  ( -1.000000000000000000, -0.000000000000000000, -0.000000000000000000 ) ) ;
#2771=FACE_BOUND ( 'NONE', #2110, .T. ) ;
#2782=ORIENTED_EDGE ( 'NONE', *, *, #1608, .F. ) ;
#2788=AXIS2_PLACEMENT_3D ( 'NONE', #4582, #4609, #3231 ) ;
#2790=ADVANCED_FACE ( 'NONE', ( #3344 ), #4746, .T. ) ;
#2794=CARTESIAN_POINT ( 'NONE',  ( 2.400000000000000799, 2.449293598294705428E-16, -1.999999999999999112 ) ) ;
#2798=ORIENTED_EDGE ( 'NONE', *, *, #975, .F. ) ;
#2807=VERTEX_POINT ( 'NONE', #5449 ) ;
#2826=AXIS2_PLACEMENT_3D ( 'NONE', #1665, #5150, #4287 ) ;
#2830=DIRECTION ( 'NONE',  ( -0.000000000000000000, 0.4999999999999998890, -0.8660254037844387076 ) ) ;
#2832=ADVANCED_FACE ( 'NONE', ( #1503, #5481 ), #3267, .F. ) ;
#2834=VECTOR ( 'NONE', #4047, 1000.000000000000000 ) ;
#2847=DIRECTION ( 'NONE',  ( -1.000000000000000000, 0.000000000000000000, -0.000000000000000000 ) ) ;
#2874=VERTEX_POINT ( 'NONE', #240 ) ;
#2879=DIRECTION ( 'NONE',  ( 0.000000000000000000, 1.224646799147353207E-16, -1.000000000000000000 ) ) ;
#2881=CARTESIAN_POINT ( 'NONE',  ( 1.300000000000000044, -0.7216878364870318308, -1.250000000000000000 ) ) ;
#2917=LINE ( 'NONE', #1163, #4262 ) ;
#2919=LINE ( 'NONE', #2051, #3181 ) ;
#2937=CARTESIAN_POINT ( 'NONE',  ( 1.300000000000000044, 0.7216878364870328300, 1.249999999999999778 ) ) ;
#2953=VERTEX_POINT ( 'NONE', #3722 ) ;
#2968=ORIENTED_EDGE ( 'NONE', *, *, #1177, .T. ) ;
#2976=ORIENTED_EDGE ( 'NONE', *, *, #224, .F. ) ;
#2981=EDGE_CURVE ( 'NONE', #4872, #3918, #4218, .T. ) ;
#2984=AXIS2_PLACEMENT_3D ( 'NONE', #3448, #430, #5241 ) ;
#2985=ORIENTED_EDGE ( 'NONE', *, *, #3745, .T. ) ;
#2989=( LENGTH_UNIT ( ) NAMED_UNIT ( * ) SI_UNIT ( .MILLI., .METRE. ) );
#2996=AXIS2_PLACEMENT_3D ( 'NONE', #2562, #1699, #3453 ) ;
#2997=DIRECTION ( 'NONE',  ( 0.000000000000000000, 0.000000000000000000, 1.000000000000000000 ) ) ;
#3000=DIRECTION ( 'NONE',  ( 0.000000000000000000, 0.000000000000000000, 1.000000000000000000 ) ) ;
#3001=ORIENTED_EDGE ( 'NONE', *, *, #257, .T. ) ;
#3010=EDGE_CURVE ( 'NONE', #11, #1449, #2919, .T. ) ;
#3017=DIRECTION ( 'NONE',  ( 0.000000000000000000, 0.000000000000000000, 1.000000000000000000 ) ) ;
#3019=EDGE_LOOP ( 'NONE', ( #1104, #4323, #609, #5026, #2026 ) ) ;
#3021=CONICAL_SURFACE ( 'NONE', #5314, 1732.050807568856271, 1.047197551196592524 ) ;
#3024=PRODUCT_CONTEXT ( 'NONE', #2071, 'mechanical' ) ;
#3030=CARTESIAN_POINT ( 'NONE',  ( 0.000000000000000000, 0.7216878364870328300, -1.250000000000000000 ) ) ;
#3032=ORIENTED_EDGE ( 'NONE', *, *, #4813, .T. ) ;
#3035=CARTESIAN_POINT ( 'NONE',  ( 0.000000000000000000, 0.7216878364870328300, 1.249999999999999778 ) ) ;
#3038=ORIENTED_EDGE ( 'NONE', *, *, #3592, .F. ) ;
#3045=EDGE_CURVE ( 'NONE', #2508, #5647, #4723, .T. ) ;
#3048=ADVANCED_FACE ( 'NONE', ( #787 ), #422, .T. ) ;
#3066=EDGE_LOOP ( 'NONE', ( #1884, #780, #4998, #5503 ) ) ;
#3089=LINE ( 'NONE', #1327, #981 ) ;
#3095=ORIENTED_EDGE ( 'NONE', *, *, #5283, .T. ) ;
#3103=VECTOR ( 'NONE', #1224, 1000.000000000000000 ) ;
#3107=AXIS2_PLACEMENT_3D ( 'NONE', #1107, #5451, #272 ) ;
#3121=DIRECTION ( 'NONE',  ( 0.000000000000000000, 0.000000000000000000, 1.000000000000000000 ) ) ;
#3144=ORIENTED_EDGE ( 'NONE', *, *, #1806, .F. ) ;
#3151=CARTESIAN_POINT ( 'NONE',  ( 1.300000000000000044, -1.082531754730548412, -0.6249999999999997780 ) ) ;
#3172=CARTESIAN_POINT ( 'NONE',  ( 2.200000000000000622, 0.000000000000000000, 0.000000000000000000 ) ) ;
#3173=ADVANCED_FACE ( 'NONE', ( #2139 ), #3866, .T. ) ;
#3181=VECTOR ( 'NONE', #2487, 1000.000000000000114 ) ;
#3192=ORIENTED_EDGE ( 'NONE', *, *, #2134, .T. ) ;
#3201=CIRCLE ( 'NONE', #2826, 3.799999999999999378 ) ;
#3203=LINE ( 'NONE', #4603, #1176 ) ;
#3226=CARTESIAN_POINT ( 'NONE',  ( 3.885274725274726393, -8.673617379884035472E-16, 0.000000000000000000 ) ) ;
#3231=DIRECTION ( 'NONE',  ( -0.000000000000000000, 0.000000000000000000, 1.000000000000000000 ) ) ;
#3239=CARTESIAN_POINT ( 'NONE',  ( 1.300000000000000044, 0.000000000000000000, 0.000000000000000000 ) ) ;
#3246=DIRECTION ( 'NONE',  ( -1.000000000000000000, -0.000000000000000000, -0.000000000000000000 ) ) ;
#3255=CIRCLE ( 'NONE', #2329, 1.610000000000000098 ) ;
#3260=CARTESIAN_POINT ( 'NONE',  ( 9.809999999999998721, 2.449293598294705921E-16, -1.999999999999999556 ) ) ;
#3263=VECTOR ( 'NONE', #1205, 1000.000000000000000 ) ;
#3267=PLANE ( 'NONE',  #1892 ) ;
#3269=FACE_OUTER_BOUND ( 'NONE', #1281, .T. ) ;
#3274=ORIENTED_EDGE ( 'NONE', *, *, #866, .F. ) ;
#3276=DIRECTION ( 'NONE',  ( -1.000000000000000000, 0.000000000000000000, 0.000000000000000000 ) ) ;
#3288=ORIENTED_EDGE ( 'NONE', *, *, #1667, .T. ) ;
#3293=AXIS2_PLACEMENT_3D ( 'NONE', #3239, #995, #1830 ) ;
#3317=ORIENTED_EDGE ( 'NONE', *, *, #5186, .F. ) ;
#3318=PLANE ( 'NONE',  #3828 ) ;
#3326=EDGE_LOOP ( 'NONE', ( #1197, #987, #3483 ) ) ;
#3344=FACE_OUTER_BOUND ( 'NONE', #3326, .T. ) ;
#3355=LINE ( 'NONE', #4220, #2456 ) ;
#3374=CARTESIAN_POINT ( 'NONE',  ( 1.300000000000000044, -0.7216878364870318308, 1.249999999999999778 ) ) ;
#3375=FACE_OUTER_BOUND ( 'NONE', #4645, .T. ) ;
#3391=EDGE_CURVE ( 'NONE', #2508, #2807, #4464, .T. ) ;
#3395=LINE ( 'NONE', #5147, #3263 ) ;
#3401=PLANE ( 'NONE',  #5477 ) ;
#3418=DIRECTION ( 'NONE',  ( 0.000000000000000000, 0.000000000000000000, -1.000000000000000000 ) ) ;
#3429=DIRECTION ( 'NONE',  ( 0.000000000000000000, 0.000000000000000000, 1.000000000000000000 ) ) ;
#3438=PRODUCT_DEFINITION_CONTEXT ( 'detailed design', #2662, 'design' ) ;
#3439=DIRECTION ( 'NONE',  ( -1.000000000000000000, -0.000000000000000000, -0.000000000000000000 ) ) ;
#3448=CARTESIAN_POINT ( 'NONE',  ( -997.9783121635130101, 0.000000000000000000, 0.000000000000000000 ) ) ;
#3453=DIRECTION ( 'NONE',  ( 0.000000000000000000, 0.000000000000000000, 1.000000000000000000 ) ) ;
#3460=CIRCLE ( 'NONE', #1443, 1.899999999999999689 ) ;
#3462=VERTEX_POINT ( 'NONE', #1067 ) ;
#3472=AXIS2_PLACEMENT_3D ( 'NONE', #4574, #634, #2385 ) ;
#3480=LINE ( 'NONE', #3597, #3707 ) ;
#3483=ORIENTED_EDGE ( 'NONE', *, *, #3391, .F. ) ;
#3488=CARTESIAN_POINT ( 'NONE',  ( 1.300000000000000044, -1.443375672974063884, -3.691112476943992763E-18 ) ) ;
#3489=EDGE_LOOP ( 'NONE', ( #5345, #64, #460, #17, #557 ) ) ;
#3502=SHAPE_DEFINITION_REPRESENTATION ( #1966, #1362 ) ;
#3508=DIRECTION ( 'NONE',  ( 0.000000000000000000, 1.000000000000000000, 0.000000000000000000 ) ) ;
#3512=COLOUR_RGB ( '',1.000000000000000000, 0.9490196078431372140, 0.9098039215686274384 ) ;
#3535=DIRECTION ( 'NONE',  ( -0.000000000000000000, -0.5000000000000002220, 0.8660254037844384856 ) ) ;
#3545=CIRCLE ( 'NONE', #5664, 4.324969328314201888 ) ;
#3552=DIRECTION ( 'NONE',  ( -0.000000000000000000, 1.000000000000000000, -0.000000000000000000 ) ) ;
#3555=EDGE_CURVE ( 'NONE', #1462, #2377, #608, .T. ) ;
#3572=CARTESIAN_POINT ( 'NONE',  ( 1.300000000000000044, 1.082531754730548856, -0.6250000000000003331 ) ) ;
#3592=EDGE_CURVE ( 'NONE', #73, #5180, #4380, .T. ) ;
#3597=CARTESIAN_POINT ( 'NONE',  ( 1.300000000000000044, -0.7216878364870318308, -1.250000000000000000 ) ) ;
#3602=CARTESIAN_POINT ( 'NONE',  ( 10.20000000000000107, 2.210487472460972205E-16, -1.610000000000000098 ) ) ;
#3614=FACE_OUTER_BOUND ( 'NONE', #1248, .T. ) ;
#3620=CIRCLE ( 'NONE', #4906, 1.999999999999999112 ) ;
#3633=VECTOR ( 'NONE', #4718, 1000.000000000000000 ) ;
#3637=ADVANCED_FACE ( 'NONE', ( #5470 ), #1526, .T. ) ;
#3645=VECTOR ( 'NONE', #1096, 1000.000000000000000 ) ;
#3651=AXIS2_PLACEMENT_3D ( 'NONE', #712, #2401, #1077 ) ;
#3670=DIRECTION ( 'NONE',  ( 0.000000000000000000, 0.000000000000000000, 1.000000000000000000 ) ) ;
#3676=DIRECTION ( 'NONE',  ( -1.000000000000000000, -0.000000000000000000, -0.000000000000000000 ) ) ;
#3678=EDGE_CURVE ( 'NONE', #2953, #4241, #3545, .T. ) ;
#3682=DIRECTION ( 'NONE',  ( -1.000000000000000000, -0.000000000000000000, -0.000000000000000000 ) ) ;
#3686=ORIENTED_EDGE ( 'NONE', *, *, #257, .F. ) ;
#3698=EDGE_LOOP ( 'NONE', ( #3902, #4264, #4387, #4835, #2362 ) ) ;
#3707=VECTOR ( 'NONE', #1839, 1000.000000000000000 ) ;
#3712=CARTESIAN_POINT ( 'NONE',  ( 1.300000000000000044, -0.7216878364870318308, 1.249999999999999778 ) ) ;
#3715=AXIS2_PLACEMENT_3D ( 'NONE', #2321, #3246, #657 ) ;
#3717=EDGE_CURVE ( 'NONE', #5180, #73, #4286, .T. ) ;
#3719=DIRECTION ( 'NONE',  ( -1.000000000000000000, 0.000000000000000000, 0.000000000000000000 ) ) ;
#3722=CARTESIAN_POINT ( 'NONE',  ( 1.820000000000000062, -3.800000000000000266, -4.653657836759940757E-16 ) ) ;
#3723=VERTEX_POINT ( 'NONE', #3916 ) ;
#3724=LINE ( 'NONE', #1940, #2357 ) ;
#3733=CLOSED_SHELL ( 'NONE', ( #2008, #4770, #3048, #962, #5652, #5302, #88, #4085, #2235, #2832, #3173, #3637, #5081, #910, #4338, #124, #853, #1705, #2616, #383, #2061, #850, #2618, #3931, #4314, #2790, #4875 ) ) ;
#3742=CARTESIAN_POINT ( 'NONE',  ( 2.021687836487040535, 0.000000000000000000, 2.168404344971008868E-16 ) ) ;
#3745=EDGE_CURVE ( 'NONE', #1983, #5180, #2530, .T. ) ;
#3755=ORIENTED_EDGE ( 'NONE', *, *, #3678, .T. ) ;
#3756=DIRECTION ( 'NONE',  ( -0.000000000000000000, -0.5000000000000002220, 0.8660254037844384856 ) ) ;
#3787=EDGE_CURVE ( 'NONE', #2713, #3462, #1623, .T. ) ;
#3804=CIRCLE ( 'NONE', #309, 1.899999999999999689 ) ;
#3811=DIRECTION ( 'NONE',  ( 0.000000000000000000, -1.224646799147353207E-16, 1.000000000000000000 ) ) ;
#3819=ORIENTED_EDGE ( 'NONE', *, *, #1553, .T. ) ;
#3822=SURFACE_STYLE_USAGE ( .BOTH. , #4625 ) ;
#3828=AXIS2_PLACEMENT_3D ( 'NONE', #1532, #1037, #151 ) ;
#3839=PRODUCT_DEFINITION ( 'UNKNOWN', '', #4982, #3438 ) ;
#3841=VERTEX_POINT ( 'NONE', #3885 ) ;
#3852=CARTESIAN_POINT ( 'NONE',  ( 2.200000000000000622, 0.000000000000000000, 2.199999999999999289 ) ) ;
#3865=ORIENTED_EDGE ( 'NONE', *, *, #3555, .T. ) ;
#3866=CYLINDRICAL_SURFACE ( 'NONE', #601, 1.999999999999999112 ) ;
#3868=DIRECTION ( 'NONE',  ( -1.000000000000000000, -0.000000000000000000, -0.000000000000000000 ) ) ;
#3874=EDGE_LOOP ( 'NONE', ( #5360, #1627 ) ) ;
#3879=DIRECTION ( 'NONE',  ( -1.000000000000000000, -0.000000000000000000, -0.000000000000000000 ) ) ;
#3885=CARTESIAN_POINT ( 'NONE',  ( 1.820000000000000062, 4.653657836759941744E-16, -3.799999999999999378 ) ) ;
#3887=VERTEX_POINT ( 'NONE', #3374 ) ;
#3889=CARTESIAN_POINT ( 'NONE',  ( 1.300000000000000044, 1.443375672974065216, 7.017607234860990640E-28 ) ) ;
#3891=DIRECTION ( 'NONE',  ( 0.000000000000000000, 0.4999999999999999445, 0.8660254037844387076 ) ) ;
#3902=ORIENTED_EDGE ( 'NONE', *, *, #5588, .F. ) ;
#3916=CARTESIAN_POINT ( 'NONE',  ( 1.300000000000000044, 0.7216878364870328300, -1.250000000000000000 ) ) ;
#3918=VERTEX_POINT ( 'NONE', #3030 ) ;
#3931=ADVANCED_FACE ( 'NONE', ( #4261 ), #3401, .T. ) ;
#3939=EDGE_LOOP ( 'NONE', ( #4330, #1677, #2985, #3038 ) ) ;
#3944=DIRECTION ( 'NONE',  ( 0.000000000000000000, 0.000000000000000000, 1.000000000000000000 ) ) ;
#3945=ORIENTED_EDGE ( 'NONE', *, *, #2981, .T. ) ;
#3958=ORIENTED_EDGE ( 'NONE', *, *, #224, .T. ) ;
#3960=CARTESIAN_POINT ( 'NONE',  ( 10.20000000000000107, 0.000000000000000000, 1.610000000000000098 ) ) ;
#3965=FACE_OUTER_BOUND ( 'NONE', #12, .T. ) ;
#3967=DIRECTION ( 'NONE',  ( -0.000000000000000000, -0.4999999999999999445, -0.8660254037844387076 ) ) ;
#3970=EDGE_LOOP ( 'NONE', ( #4086, #4777, #2312 ) ) ;
#3977=ORIENTED_EDGE ( 'NONE', *, *, #93, .T. ) ;
#3981=CARTESIAN_POINT ( 'NONE',  ( 2.400000000000000799, 0.000000000000000000, 0.000000000000000000 ) ) ;
#3989=TOROIDAL_SURFACE ( 'NONE', #2430, 2.199999999999999289, 0.2000000000000000111 ) ;
#4016=AXIS2_PLACEMENT_3D ( 'NONE', #2511, #3868, #380 ) ;
#4047=DIRECTION ( 'NONE',  ( -0.000000000000000000, -1.000000000000000000, -0.000000000000000000 ) ) ;
#4059=EDGE_CURVE ( 'NONE', #5593, #928, #3620, .T. ) ;
#4060=DIRECTION ( 'NONE',  ( 0.000000000000000000, 0.000000000000000000, 1.000000000000000000 ) ) ;
#4062=EDGE_CURVE ( 'NONE', #1449, #4872, #3480, .T. ) ;
#4085=ADVANCED_FACE ( 'NONE', ( #457 ), #2216, .T. ) ;
#4086=ORIENTED_EDGE ( 'NONE', *, *, #4657, .F. ) ;
#4090=EDGE_CURVE ( 'NONE', #3887, #2508, #2650, .T. ) ;
#4093=CYLINDRICAL_SURFACE ( 'NONE', #2622, 3.799999999999999378 ) ;
#4098=DIRECTION ( 'NONE',  ( -0.000000000000000000, 1.000000000000000000, -0.000000000000000000 ) ) ;
#4101=AXIS2_PLACEMENT_3D ( 'NONE', #1448, #2681, #5306 ) ;
#4109=EDGE_CURVE ( 'NONE', #1307, #2597, #543, .T. ) ;
#4112=ORIENTED_EDGE ( 'NONE', *, *, #446, .F. ) ;
#4123=DIRECTION ( 'NONE',  ( -1.000000000000000000, -0.000000000000000000, -0.000000000000000000 ) ) ;
#4133=PLANE ( 'NONE',  #4847 ) ;
#4149=DIRECTION ( 'NONE',  ( -1.000000000000000000, -0.000000000000000000, -0.000000000000000000 ) ) ;
#4152=FACE_OUTER_BOUND ( 'NONE', #3019, .T. ) ;
#4167=ORIENTED_EDGE ( 'NONE', *, *, #1817, .T. ) ;
#4169=DIRECTION ( 'NONE',  ( -1.000000000000000000, -0.000000000000000000, -0.000000000000000000 ) ) ;
#4172=ORIENTED_EDGE ( 'NONE', *, *, #4109, .T. ) ;
#4182=DIRECTION ( 'NONE',  ( -1.000000000000000000, -0.000000000000000000, -0.000000000000000000 ) ) ;
#4187=AXIS2_PLACEMENT_3D ( 'NONE', #2590, #1214, #4263 ) ;
#4205=CARTESIAN_POINT ( 'NONE',  ( 0.000000000000000000, 2.449293598294705428E-16, -1.999999999999999112 ) ) ;
#4209=DIRECTION ( 'NONE',  ( 0.000000000000000000, 0.000000000000000000, 1.000000000000000000 ) ) ;
#4218=LINE ( 'NONE', #2027, #4921 ) ;
#4220=CARTESIAN_POINT ( 'NONE',  ( 1.300000000000000044, 0.7216878364870328300, 1.249999999999999778 ) ) ;
#4224=EDGE_CURVE ( 'NONE', #5647, #4643, #2917, .T. ) ;
#4232=EDGE_CURVE ( 'NONE', #1931, #11, #2514, .T. ) ;
#4234=DIRECTION ( 'NONE',  ( -0.5000000000000044409, 1.060575238724903587E-16, -0.8660254037844360431 ) ) ;
#4237=CARTESIAN_POINT ( 'NONE',  ( 0.000000000000000000, 0.000000000000000000, 0.000000000000000000 ) ) ;
#4241=VERTEX_POINT ( 'NONE', #1567 ) ;
#4243=ORIENTED_EDGE ( 'NONE', *, *, #2646, .F. ) ;
#4261=FACE_OUTER_BOUND ( 'NONE', #3970, .T. ) ;
#4262=VECTOR ( 'NONE', #3719, 1000.000000000000000 ) ;
#4263=DIRECTION ( 'NONE',  ( 0.000000000000000000, 0.5000000000000002220, -0.8660254037844384856 ) ) ;
#4264=ORIENTED_EDGE ( 'NONE', *, *, #2646, .T. ) ;
#4269=CARTESIAN_POINT ( 'NONE',  ( 1.300000000000000044, 0.000000000000000000, 0.000000000000000000 ) ) ;
#4274=EDGE_LOOP ( 'NONE', ( #4581, #3819, #4596, #4818, #2798 ) ) ;
#4286=CIRCLE ( 'NONE', #515, 1.999999999999999556 ) ;
#4287=DIRECTION ( 'NONE',  ( 0.000000000000000000, 0.000000000000000000, 1.000000000000000000 ) ) ;
#4296=CARTESIAN_POINT ( 'NONE',  ( 1.820000000000000062, 0.000000000000000000, 0.000000000000000000 ) ) ;
#4314=ADVANCED_FACE ( 'NONE', ( #2137 ), #1365, .T. ) ;
#4322=FACE_OUTER_BOUND ( 'NONE', #700, .T. ) ;
#4323=ORIENTED_EDGE ( 'NONE', *, *, #800, .T. ) ;
#4330=ORIENTED_EDGE ( 'NONE', *, *, #598, .F. ) ;
#4338=ADVANCED_FACE ( 'NONE', ( #2538 ), #5646, .T. ) ;
#4349=VERTEX_POINT ( 'NONE', #5187 ) ;
#4357=EDGE_LOOP ( 'NONE', ( #4782, #3865, #5509, #1258, #552 ) ) ;
#4361=VECTOR ( 'NONE', #3535, 1000.000000000000114 ) ;
#4365=VECTOR ( 'NONE', #3552, 1000.000000000000000 ) ;
#4380=CIRCLE ( 'NONE', #330, 1.999999999999999556 ) ;
#4383=VECTOR ( 'NONE', #60, 1000.000000000000000 ) ;
#4387=ORIENTED_EDGE ( 'NONE', *, *, #4232, .T. ) ;
#4388=ORIENTED_EDGE ( 'NONE', *, *, #5169, .T. ) ;
#4401=CARTESIAN_POINT ( 'NONE',  ( 1.300000000000000044, 0.7216878364870328300, 1.249999999999999778 ) ) ;
#4410=VERTEX_POINT ( 'NONE', #1758 ) ;
#4429=CARTESIAN_POINT ( 'NONE',  ( 1.300000000000000044, -0.7216878364870318308, -1.250000000000000000 ) ) ;
#4447=FACE_OUTER_BOUND ( 'NONE', #3698, .T. ) ;
#4456=CIRCLE ( 'NONE', #4918, 1.249999999999999778 ) ;
#4464=CIRCLE ( 'NONE', #4101, 1.249999999999999778 ) ;
#4467=VERTEX_POINT ( 'NONE', #3035 ) ;
#4486=CARTESIAN_POINT ( 'NONE',  ( 2.200000000000000622, 0.000000000000000000, 0.000000000000000000 ) ) ;
#4504=VERTEX_POINT ( 'NONE', #3602 ) ;
#4506=DIRECTION ( 'NONE',  ( 0.000000000000000000, 0.000000000000000000, 1.000000000000000000 ) ) ;
#4514=LINE ( 'NONE', #1894, #691 ) ;
#4531=ORIENTED_EDGE ( 'NONE', *, *, #800, .F. ) ;
#4545=CARTESIAN_POINT ( 'NONE',  ( 1.820000000000000062, 0.000000000000000000, 0.000000000000000000 ) ) ;
#4550=CARTESIAN_POINT ( 'NONE',  ( 8.673617379884035472E-16, 0.000000000000000000, 0.000000000000000000 ) ) ;
#4574=CARTESIAN_POINT ( 'NONE',  ( 1.300000000000000044, 1.443375672974065216, 7.017607234860990640E-28 ) ) ;
#4581=ORIENTED_EDGE ( 'NONE', *, *, #2197, .T. ) ;
#4582=CARTESIAN_POINT ( 'NONE',  ( 4.336808689942017736E-16, 0.000000000000000000, 0.000000000000000000 ) ) ;
#4592=DIRECTION ( 'NONE',  ( 1.000000000000000000, 0.000000000000000000, -0.000000000000000000 ) ) ;
#4596=ORIENTED_EDGE ( 'NONE', *, *, #149, .T. ) ;
#4599=PLANE ( 'NONE',  #4726 ) ;
#4603=CARTESIAN_POINT ( 'NONE',  ( 1.300000000000000044, -0.7216878364870318308, 1.249999999999999778 ) ) ;
#4605=DIRECTION ( 'NONE',  ( 0.000000000000000000, 0.000000000000000000, 1.000000000000000000 ) ) ;
#4609=DIRECTION ( 'NONE',  ( -1.000000000000000000, 0.000000000000000000, -0.000000000000000000 ) ) ;
#4616=ORIENTED_EDGE ( 'NONE', *, *, #3745, .F. ) ;
#4617=LINE ( 'NONE', #676, #5577 ) ;
#4625=SURFACE_SIDE_STYLE ('',( #2470 ) ) ;
#4634=DIRECTION ( 'NONE',  ( -1.000000000000000000, -0.000000000000000000, -0.000000000000000000 ) ) ;
#4639=VECTOR ( 'NONE', #1093, 1000.000000000000114 ) ;
#4643=VERTEX_POINT ( 'NONE', #823 ) ;
#4645=EDGE_LOOP ( 'NONE', ( #1736, #4172, #5259, #3274, #4671 ) ) ;
#4657=EDGE_CURVE ( 'NONE', #1449, #1931, #385, .T. ) ;
#4666=CARTESIAN_POINT ( 'NONE',  ( 2.400000000000000799, 0.000000000000000000, 0.000000000000000000 ) ) ;
#4671=ORIENTED_EDGE ( 'NONE', *, *, #5090, .F. ) ;
#4686=EDGE_CURVE ( 'NONE', #1983, #4504, #3255, .T. ) ;
#4689=DIRECTION ( 'NONE',  ( -1.000000000000000000, 0.000000000000000000, 0.000000000000000000 ) ) ;
#4691=PLANE ( 'NONE',  #5211 ) ;
#4698=CARTESIAN_POINT ( 'NONE',  ( 0.000000000000000000, 0.000000000000000000, 0.000000000000000000 ) ) ;
#4699=ORIENTED_EDGE ( 'NONE', *, *, #4224, .F. ) ;
#4713=DIRECTION ( 'NONE',  ( -1.000000000000000000, -0.000000000000000000, -0.000000000000000000 ) ) ;
#4718=DIRECTION ( 'NONE',  ( -0.000000000000000000, 0.5000000000000001110, 0.8660254037844385966 ) ) ;
#4723=LINE ( 'NONE', #5251, #1156 ) ;
#4724=ORIENTED_EDGE ( 'NONE', *, *, #3592, .T. ) ;
#4726=AXIS2_PLACEMENT_3D ( 'NONE', #1085, #2847, #107 ) ;
#4738=VECTOR ( 'NONE', #2041, 1000.000000000000000 ) ;
#4746=PLANE ( 'NONE',  #2996 ) ;
#4757=DIRECTION ( 'NONE',  ( 0.000000000000000000, 0.000000000000000000, -1.000000000000000000 ) ) ;
#4762=CARTESIAN_POINT ( 'NONE',  ( 1.300000000000000044, 0.7216878364870328300, -1.250000000000000000 ) ) ;
#4770=ADVANCED_FACE ( 'NONE', ( #1742 ), #3989, .F. ) ;
#4775=DIRECTION ( 'NONE',  ( -1.000000000000000000, 0.000000000000000000, 0.000000000000000000 ) ) ;
#4777=ORIENTED_EDGE ( 'NONE', *, *, #3010, .F. ) ;
#4782=ORIENTED_EDGE ( 'NONE', *, *, #2389, .T. ) ;
#4783=CARTESIAN_POINT ( 'NONE',  ( 10.20000000000000107, 0.000000000000000000, 0.000000000000000000 ) ) ;
#4810=ORIENTED_EDGE ( 'NONE', *, *, #4657, .T. ) ;
#4813=EDGE_CURVE ( 'NONE', #4349, #4241, #3804, .T. ) ;
#4818=ORIENTED_EDGE ( 'NONE', *, *, #2118, .F. ) ;
#4819=DIRECTION ( 'NONE',  ( 0.000000000000000000, 0.000000000000000000, 1.000000000000000000 ) ) ;
#4831=CARTESIAN_POINT ( 'NONE',  ( 2.400000000000000799, 0.000000000000000000, 0.000000000000000000 ) ) ;
#4835=ORIENTED_EDGE ( 'NONE', *, *, #2442, .T. ) ;
#4836=CIRCLE ( 'NONE', #5574, 3.799999999999999378 ) ;
#4847=AXIS2_PLACEMENT_3D ( 'NONE', #215, #1969, #4592 ) ;
#4872=VERTEX_POINT ( 'NONE', #917 ) ;
#4875=ADVANCED_FACE ( 'NONE', ( #3965 ), #1693, .F. ) ;
#4906=AXIS2_PLACEMENT_3D ( 'NONE', #4831, #5688, #2189 ) ;
#4907=LINE ( 'NONE', #1916, #2834 ) ;
#4918=AXIS2_PLACEMENT_3D ( 'NONE', #2534, #813, #3429 ) ;
#4921=VECTOR ( 'NONE', #5510, 1000.000000000000000 ) ;
#4936=TOROIDAL_SURFACE ( 'NONE', #3651, 2.199999999999999289, 0.2000000000000000111 ) ;
#4956=FACE_OUTER_BOUND ( 'NONE', #5098, .T. ) ;
#4974=CARTESIAN_POINT ( 'NONE',  ( 3.885274725274726393, -8.673617379884035472E-16, 0.000000000000000000 ) ) ;
#4982=PRODUCT_DEFINITION_FORMATION_WITH_SPECIFIED_SOURCE ( 'ANY', '', #2062, .NOT_KNOWN. ) ;
#4998=ORIENTED_EDGE ( 'NONE', *, *, #1122, .T. ) ;
#5001=FACE_OUTER_BOUND ( 'NONE', #4357, .T. ) ;
#5011=FACE_OUTER_BOUND ( 'NONE', #1759, .T. ) ;
#5021=DIRECTION ( 'NONE',  ( -1.000000000000000000, 0.000000000000000000, 0.000000000000000000 ) ) ;
#5025=AXIS2_PLACEMENT_3D ( 'NONE', #2141, #2111, #4757 ) ;
#5026=ORIENTED_EDGE ( 'NONE', *, *, #1667, .F. ) ;
#5037=CARTESIAN_POINT ( 'NONE',  ( 9.809999999999998721, 0.000000000000000000, 0.000000000000000000 ) ) ;
#5049=FACE_OUTER_BOUND ( 'NONE', #1360, .T. ) ;
#5059=ORIENTED_EDGE ( 'NONE', *, *, #5186, .T. ) ;
#5067=LINE ( 'NONE', #703, #1609 ) ;
#5075=FACE_OUTER_BOUND ( 'NONE', #3066, .T. ) ;
#5081=ADVANCED_FACE ( 'NONE', ( #1026 ), #4599, .F. ) ;
#5085=DIRECTION ( 'NONE',  ( 0.000000000000000000, 1.000000000000000000, 0.000000000000000000 ) ) ;
#5090=EDGE_CURVE ( 'NONE', #2377, #1059, #5347, .T. ) ;
#5098=EDGE_LOOP ( 'NONE', ( #3977, #632, #1923, #1653, #4699 ) ) ;
#5104=EDGE_CURVE ( 'NONE', #5494, #1387, #1049, .T. ) ;
#5109=EDGE_CURVE ( 'NONE', #4504, #1983, #5286, .T. ) ;
#5111=LINE ( 'NONE', #1133, #159 ) ;
#5119=CARTESIAN_POINT ( 'NONE',  ( 3.885274725274726393, -8.673617379884035472E-16, 0.000000000000000000 ) ) ;
#5121=( NAMED_UNIT ( * ) PLANE_ANGLE_UNIT ( ) SI_UNIT ( $, .RADIAN. ) );
#5129=PLANE ( 'NONE',  #4187 ) ;
#5147=CARTESIAN_POINT ( 'NONE',  ( 0.000000000000000000, 0.000000000000000000, 3.799999999999999378 ) ) ;
#5150=DIRECTION ( 'NONE',  ( -1.000000000000000000, -0.000000000000000000, -0.000000000000000000 ) ) ;
#5156=DIRECTION ( 'NONE',  ( -1.000000000000000000, 0.000000000000000000, -0.000000000000000000 ) ) ;
#5161=DIRECTION ( 'NONE',  ( 0.000000000000000000, 0.000000000000000000, 1.000000000000000000 ) ) ;
#5167=ORIENTED_EDGE ( 'NONE', *, *, #3555, .F. ) ;
#5169=EDGE_CURVE ( 'NONE', #1307, #1462, #1237, .T. ) ;
#5180=VERTEX_POINT ( 'NONE', #2380 ) ;
#5186=EDGE_CURVE ( 'NONE', #5180, #928, #4514, .T. ) ;
#5187=CARTESIAN_POINT ( 'NONE',  ( 8.673617379884035472E-16, 1.899999999999999689, 0.000000000000000000 ) ) ;
#5191=CARTESIAN_POINT ( 'NONE',  ( 1.300000000000000044, 0.7216878364870328300, -1.250000000000000000 ) ) ;
#5192=VECTOR ( 'NONE', #3276, 1000.000000000000000 ) ;
#5197=DIRECTION ( 'NONE',  ( 0.000000000000000000, 0.000000000000000000, 1.000000000000000000 ) ) ;
#5203=FILL_AREA_STYLE ('',( #1206 ) ) ;
#5211=AXIS2_PLACEMENT_3D ( 'NONE', #1587, #727, #5156 ) ;
#5213=DIRECTION ( 'NONE',  ( 1.000000000000000000, 0.000000000000000000, 0.000000000000000000 ) ) ;
#5215=( GEOMETRIC_REPRESENTATION_CONTEXT ( 3 ) GLOBAL_UNCERTAINTY_ASSIGNED_CONTEXT ( ( #5354 ) ) GLOBAL_UNIT_ASSIGNED_CONTEXT ( ( #2356, #5498, #605 ) ) REPRESENTATION_CONTEXT ( 'NONE', 'WORKASPACE' ) );
#5221=CIRCLE ( 'NONE', #1637, 2.199999999999999289 ) ;
#5230=UNCERTAINTY_MEASURE_WITH_UNIT (LENGTH_MEASURE( 1.000000000000000082E-05 ), #2989, 'distance_accuracy_value', 'NONE');
#5231=DIRECTION ( 'NONE',  ( -1.000000000000000000, -0.000000000000000000, -0.000000000000000000 ) ) ;
#5241=DIRECTION ( 'NONE',  ( 0.000000000000000000, 0.000000000000000000, 1.000000000000000000 ) ) ;
#5243=CARTESIAN_POINT ( 'NONE',  ( 1.300000000000000044, -1.443375672974063884, -3.691112476943992763E-18 ) ) ;
#5251=CARTESIAN_POINT ( 'NONE',  ( 1.300000000000000044, -1.443375672974063884, -3.691112476943992763E-18 ) ) ;
#5259=ORIENTED_EDGE ( 'NONE', *, *, #975, .T. ) ;
#5283=EDGE_CURVE ( 'NONE', #4410, #4643, #223, .T. ) ;
#5286=CIRCLE ( 'NONE', #3715, 1.610000000000000098 ) ;
#5302=ADVANCED_FACE ( 'NONE', ( #5547 ), #5604, .T. ) ;
#5306=DIRECTION ( 'NONE',  ( 0.000000000000000000, 0.000000000000000000, 1.000000000000000000 ) ) ;
#5311=VECTOR ( 'NONE', #3879, 1000.000000000000000 ) ;
#5314=AXIS2_PLACEMENT_3D ( 'NONE', #421, #2180, #4819 ) ;
#5326=CARTESIAN_POINT ( 'NONE',  ( 1.300000000000000044, 1.082531754730548856, 0.6250000000000006661 ) ) ;
#5345=ORIENTED_EDGE ( 'NONE', *, *, #4090, .T. ) ;
#5347=LINE ( 'NONE', #1517, #5192 ) ;
#5350=CARTESIAN_POINT ( 'NONE',  ( 3.885274725274726393, -8.673617379884035472E-16, 0.000000000000000000 ) ) ;
#5352=DIRECTION ( 'NONE',  ( -1.000000000000000000, -0.000000000000000000, -0.000000000000000000 ) ) ;
#5354=UNCERTAINTY_MEASURE_WITH_UNIT (LENGTH_MEASURE( 1.000000000000000082E-05 ), #2356, 'distance_accuracy_value', 'NONE');
#5360=ORIENTED_EDGE ( 'NONE', *, *, #4686, .F. ) ;
#5369=AXIS2_PLACEMENT_3D ( 'NONE', #4269, #5479, #212 ) ;
#5370=PLANE ( 'NONE',  #2553 ) ;
#5376=VERTEX_POINT ( 'NONE', #252 ) ;
#5383=ORIENTED_EDGE ( 'NONE', *, *, #4059, .T. ) ;
#5402=CIRCLE ( 'NONE', #619, 4.324969328314201888 ) ;
#5413=CARTESIAN_POINT ( 'NONE',  ( 0.000000000000000000, 0.000000000000000000, 0.000000000000000000 ) ) ;
#5434=ORIENTED_EDGE ( 'NONE', *, *, #3787, .T. ) ;
#5436=DIRECTION ( 'NONE',  ( -0.000000000000000000, -1.000000000000000000, -0.000000000000000000 ) ) ;
#5443=( GEOMETRIC_REPRESENTATION_CONTEXT ( 3 ) GLOBAL_UNCERTAINTY_ASSIGNED_CONTEXT ( ( #1255 ) ) GLOBAL_UNIT_ASSIGNED_CONTEXT ( ( #1086, #742, #1689 ) ) REPRESENTATION_CONTEXT ( 'NONE', 'WORKASPACE' ) );
#5449=CARTESIAN_POINT ( 'NONE',  ( 1.300000000000000044, 0.000000000000000000, 1.249999999999999778 ) ) ;
#5451=DIRECTION ( 'NONE',  ( -1.000000000000000000, -0.000000000000000000, -0.000000000000000000 ) ) ;
#5454=EDGE_CURVE ( 'NONE', #2713, #5376, #3395, .T. ) ;
#5470=FACE_OUTER_BOUND ( 'NONE', #3939, .T. ) ;
#5477=AXIS2_PLACEMENT_3D ( 'NONE', #1645, #4775, #2589 ) ;
#5479=DIRECTION ( 'NONE',  ( -1.000000000000000000, -0.000000000000000000, -0.000000000000000000 ) ) ;
#5481=FACE_OUTER_BOUND ( 'NONE', #501, .T. ) ;
#5488=STYLED_ITEM('',(#5730),#698);
#5494=VERTEX_POINT ( 'NONE', #3852 ) ;
#5497=DIRECTION ( 'NONE',  ( 0.000000000000000000, 0.000000000000000000, 1.000000000000000000 ) ) ;
#5498=( NAMED_UNIT ( * ) PLANE_ANGLE_UNIT ( ) SI_UNIT ( $, .RADIAN. ) );
#5499=FACE_OUTER_BOUND ( 'NONE', #1965, .T. ) ;
#5502=CARTESIAN_POINT ( 'NONE',  ( 1.300000000000000044, 1.443375672974065216, 7.017607234860990640E-28 ) ) ;
#5503=ORIENTED_EDGE ( 'NONE', *, *, #4059, .F. ) ;
#5509=ORIENTED_EDGE ( 'NONE', *, *, #5090, .T. ) ;
#5510=DIRECTION ( 'NONE',  ( -0.000000000000000000, 1.000000000000000000, -0.000000000000000000 ) ) ;
#5540=DIRECTION ( 'NONE',  ( -1.000000000000000000, 0.000000000000000000, 0.000000000000000000 ) ) ;
#5547=FACE_OUTER_BOUND ( 'NONE', #1391, .T. ) ;
#5559=DIRECTION ( 'NONE',  ( 0.000000000000000000, 0.000000000000000000, 1.000000000000000000 ) ) ;
#5567=ORIENTED_EDGE ( 'NONE', *, *, #1343, .F. ) ;
#5571=AXIS2_PLACEMENT_3D ( 'NONE', #1238, #4713, #778 ) ;
#5574=AXIS2_PLACEMENT_3D ( 'NONE', #5589, #1216, #349 ) ;
#5577=VECTOR ( 'NONE', #1481, 1000.000000000000000 ) ;
#5581=AXIS2_PLACEMENT_3D ( 'NONE', #2429, #5540, #3670 ) ;
#5588=EDGE_CURVE ( 'NONE', #286, #2807, #1493, .T. ) ;
#5589=CARTESIAN_POINT ( 'NONE',  ( 1.820000000000000062, 0.000000000000000000, 0.000000000000000000 ) ) ;
#5593=VERTEX_POINT ( 'NONE', #2794 ) ;
#5604=SPHERICAL_SURFACE ( 'NONE', #2433, 4.324969328314201888 ) ;
#5631=SHAPE_REPRESENTATION_RELATIONSHIP ( 'NONE' , 'NONE' ,  #1362, #622 ) ;
#5646=PLANE ( 'NONE',  #582 ) ;
#5647=VERTEX_POINT ( 'NONE', #664 ) ;
#5651=AXIS2_PLACEMENT_3D ( 'NONE', #4486, #168, #1838 ) ;
#5652=ADVANCED_FACE ( 'NONE', ( #5499 ), #4093, .T. ) ;
#5664=AXIS2_PLACEMENT_3D ( 'NONE', #4974, #2879, #2390 ) ;
#5672=ORIENTED_EDGE ( 'NONE', *, *, #4813, .F. ) ;
#5681=CARTESIAN_POINT ( 'NONE',  ( 2.400000000000000799, 2.694222958124176020E-16, -2.199999999999999289 ) ) ;
#5688=DIRECTION ( 'NONE',  ( 1.000000000000000000, 0.000000000000000000, 0.000000000000000000 ) ) ;
#5724=COLOUR_RGB('Black',0.12,0.14,0.17);
#5725=FILL_AREA_STYLE_COLOUR('',#5724);
#5726=FILL_AREA_STYLE('',(#5725));
#5727=SURFACE_STYLE_FILL_AREA(#5726);
#5728=SURFACE_SIDE_STYLE('',(#5727));
#5729=SURFACE_STYLE_USAGE(.BOTH.,#5728);
#5730=PRESENTATION_STYLE_ASSIGNMENT((#5729));
ENDSEC;
END-ISO-10303-21;
